ISO-10303-21;
HEADER;
/* Generated by software containing ST-Developer
 * from STEP Tools, Inc. (www.steptools.com) 
 */

FILE_DESCRIPTION(
/* description */ (''),
/* implementation_level */ '2;1');

FILE_NAME(
/* name */ 'Cap Screw - M5x20.step',
/* time_stamp */ '2026-10-29T16:43:51-07:00',
/* author */ (''),
/* organization */ (''),
/* preprocessor_version */ 'ST-DEVELOPER v20.2',
/* originating_system */ 'Autodesk Translation Framework v15.17.0.0',
/* authorisation */ '');

FILE_SCHEMA (('AUTOMOTIVE_DESIGN { 1 0 10303 214 3 1 1 }'));
ENDSEC;

DATA;
#10=MECHANICAL_DESIGN_GEOMETRIC_PRESENTATION_REPRESENTATION('',(#384),#10292);
#286=ORIENTED_CLOSED_SHELL('',*,#5030,.F.);
#291=BREP_WITH_VOIDS('Body1',#5029,(#286));
#311=CONICAL_SURFACE('',#5737,0.4,0.785398163397448);
#312=CONICAL_SURFACE('',#5741,0.41,0.785398163397448);
#313=CONICAL_SURFACE('',#5745,0.26,0.463647609000806);
#314=CONICAL_SURFACE('',#5749,0.225,0.785398163397448);
#338=SHAPE_REPRESENTATION_RELATIONSHIP('SRR','None',#10436,#361);
#361=ADVANCED_BREP_SHAPE_REPRESENTATION('',(#291),#10288);
#384=STYLED_ITEM('',(#10635),#291);
#525=FACE_BOUND('',#1368,.T.);
#684=PLANE('',#5735);
#685=PLANE('',#5743);
#686=PLANE('',#5751);
#687=PLANE('',#5752);
#688=PLANE('',#5753);
#689=PLANE('',#5754);
#690=PLANE('',#5755);
#691=PLANE('',#5756);
#692=PLANE('',#5757);
#693=PLANE('',#5758);
#694=PLANE('',#5759);
#956=FACE_OUTER_BOUND('',#1363,.T.);
#957=FACE_OUTER_BOUND('',#1364,.T.);
#958=FACE_OUTER_BOUND('',#1365,.T.);
#959=FACE_OUTER_BOUND('',#1366,.T.);
#960=FACE_OUTER_BOUND('',#1367,.T.);
#961=FACE_OUTER_BOUND('',#1369,.T.);
#962=FACE_OUTER_BOUND('',#1370,.T.);
#963=FACE_OUTER_BOUND('',#1371,.T.);
#964=FACE_OUTER_BOUND('',#1372,.T.);
#965=FACE_OUTER_BOUND('',#1373,.T.);
#966=FACE_OUTER_BOUND('',#1374,.T.);
#967=FACE_OUTER_BOUND('',#1375,.T.);
#968=FACE_OUTER_BOUND('',#1376,.T.);
#969=FACE_OUTER_BOUND('',#1377,.T.);
#970=FACE_OUTER_BOUND('',#1378,.T.);
#971=FACE_OUTER_BOUND('',#1379,.T.);
#972=FACE_OUTER_BOUND('',#1380,.T.);
#1363=EDGE_LOOP('',(#4485));
#1364=EDGE_LOOP('',(#4486,#4487,#4488,#4489));
#1365=EDGE_LOOP('',(#4490,#4491,#4492,#4493));
#1366=EDGE_LOOP('',(#4494,#4495,#4496,#4497));
#1367=EDGE_LOOP('',(#4498));
#1368=EDGE_LOOP('',(#4499));
#1369=EDGE_LOOP('',(#4500,#4501,#4502,#4503));
#1370=EDGE_LOOP('',(#4504,#4505,#4506,#4507));
#1371=EDGE_LOOP('',(#4508,#4509,#4510,#4511));
#1372=EDGE_LOOP('',(#4512));
#1373=EDGE_LOOP('',(#4513,#4514,#4515,#4516));
#1374=EDGE_LOOP('',(#4517,#4518,#4519,#4520));
#1375=EDGE_LOOP('',(#4521,#4522,#4523,#4524));
#1376=EDGE_LOOP('',(#4525,#4526,#4527,#4528));
#1377=EDGE_LOOP('',(#4529,#4530,#4531,#4532));
#1378=EDGE_LOOP('',(#4533,#4534,#4535,#4536));
#1379=EDGE_LOOP('',(#4537,#4538,#4539,#4540,#4541,#4542));
#1380=EDGE_LOOP('',(#4543,#4544,#4545,#4546,#4547,#4548));
#1751=LINE('',#10014,#2143);
#1752=LINE('',#10018,#2144);
#1753=LINE('',#10022,#2145);
#1754=LINE('',#10029,#2146);
#1755=LINE('',#10033,#2147);
#1756=LINE('',#10037,#2148);
#1757=LINE('',#10042,#2149);
#1758=LINE('',#10044,#2150);
#1759=LINE('',#10046,#2151);
#1760=LINE('',#10047,#2152);
#1761=LINE('',#10050,#2153);
#1762=LINE('',#10052,#2154);
#1763=LINE('',#10053,#2155);
#1764=LINE('',#10056,#2156);
#1765=LINE('',#10058,#2157);
#1766=LINE('',#10059,#2158);
#1767=LINE('',#10062,#2159);
#1768=LINE('',#10064,#2160);
#1769=LINE('',#10065,#2161);
#1770=LINE('',#10068,#2162);
#1771=LINE('',#10070,#2163);
#1772=LINE('',#10071,#2164);
#1773=LINE('',#10073,#2165);
#1774=LINE('',#10074,#2166);
#2143=VECTOR('',#7104,0.4);
#2144=VECTOR('',#7109,0.425);
#2145=VECTOR('',#7114,0.41);
#2146=VECTOR('',#7123,0.26);
#2147=VECTOR('',#7128,0.25);
#2148=VECTOR('',#7133,0.225);
#2149=VECTOR('',#7138,1.);
#2150=VECTOR('',#7139,1.);
#2151=VECTOR('',#7140,1.);
#2152=VECTOR('',#7141,1.);
#2153=VECTOR('',#7144,1.);
#2154=VECTOR('',#7145,1.);
#2155=VECTOR('',#7146,1.);
#2156=VECTOR('',#7149,1.);
#2157=VECTOR('',#7150,1.);
#2158=VECTOR('',#7151,1.);
#2159=VECTOR('',#7154,1.);
#2160=VECTOR('',#7155,1.);
#2161=VECTOR('',#7156,1.);
#2162=VECTOR('',#7159,1.);
#2163=VECTOR('',#7160,1.);
#2164=VECTOR('',#7161,1.);
#2165=VECTOR('',#7164,1.);
#2166=VECTOR('',#7165,1.);
#2370=CIRCLE('',#5736,0.375);
#2371=CIRCLE('',#5738,0.425);
#2372=CIRCLE('',#5740,0.425);
#2373=CIRCLE('',#5742,0.395);
#2374=CIRCLE('',#5744,0.27);
#2375=CIRCLE('',#5746,0.24505);
#2376=CIRCLE('',#5748,0.24505);
#2377=CIRCLE('',#5750,0.2);
#2747=VERTEX_POINT('',#10009);
#2748=VERTEX_POINT('',#10012);
#2749=VERTEX_POINT('',#10016);
#2750=VERTEX_POINT('',#10020);
#2751=VERTEX_POINT('',#10024);
#2752=VERTEX_POINT('',#10027);
#2753=VERTEX_POINT('',#10031);
#2754=VERTEX_POINT('',#10035);
#2755=VERTEX_POINT('',#10040);
#2756=VERTEX_POINT('',#10041);
#2757=VERTEX_POINT('',#10043);
#2758=VERTEX_POINT('',#10045);
#2759=VERTEX_POINT('',#10049);
#2760=VERTEX_POINT('',#10051);
#2761=VERTEX_POINT('',#10055);
#2762=VERTEX_POINT('',#10057);
#2763=VERTEX_POINT('',#10061);
#2764=VERTEX_POINT('',#10063);
#2765=VERTEX_POINT('',#10067);
#2766=VERTEX_POINT('',#10069);
#3333=EDGE_CURVE('',#2747,#2747,#2370,.T.);
#3334=EDGE_CURVE('',#2748,#2748,#2371,.T.);
#3335=EDGE_CURVE('',#2748,#2747,#1751,.T.);
#3336=EDGE_CURVE('',#2749,#2749,#2372,.T.);
#3337=EDGE_CURVE('',#2749,#2748,#1752,.T.);
#3338=EDGE_CURVE('',#2750,#2750,#2373,.T.);
#3339=EDGE_CURVE('',#2750,#2749,#1753,.T.);
#3340=EDGE_CURVE('',#2751,#2751,#2374,.T.);
#3341=EDGE_CURVE('',#2752,#2752,#2375,.F.);
#3342=EDGE_CURVE('',#2752,#2751,#1754,.T.);
#3343=EDGE_CURVE('',#2753,#2753,#2376,.F.);
#3344=EDGE_CURVE('',#2753,#2752,#1755,.T.);
#3345=EDGE_CURVE('',#2754,#2754,#2377,.T.);
#3346=EDGE_CURVE('',#2754,#2753,#1756,.T.);
#3347=EDGE_CURVE('',#2755,#2756,#1757,.T.);
#3348=EDGE_CURVE('',#2756,#2757,#1758,.T.);
#3349=EDGE_CURVE('',#2757,#2758,#1759,.T.);
#3350=EDGE_CURVE('',#2755,#2758,#1760,.T.);
#3351=EDGE_CURVE('',#2756,#2759,#1761,.T.);
#3352=EDGE_CURVE('',#2759,#2760,#1762,.T.);
#3353=EDGE_CURVE('',#2760,#2757,#1763,.T.);
#3354=EDGE_CURVE('',#2759,#2761,#1764,.T.);
#3355=EDGE_CURVE('',#2761,#2762,#1765,.T.);
#3356=EDGE_CURVE('',#2762,#2760,#1766,.T.);
#3357=EDGE_CURVE('',#2761,#2763,#1767,.T.);
#3358=EDGE_CURVE('',#2763,#2764,#1768,.T.);
#3359=EDGE_CURVE('',#2764,#2762,#1769,.T.);
#3360=EDGE_CURVE('',#2763,#2765,#1770,.T.);
#3361=EDGE_CURVE('',#2765,#2766,#1771,.T.);
#3362=EDGE_CURVE('',#2766,#2764,#1772,.T.);
#3363=EDGE_CURVE('',#2765,#2755,#1773,.T.);
#3364=EDGE_CURVE('',#2758,#2766,#1774,.T.);
#4485=ORIENTED_EDGE('',*,*,#3333,.F.);
#4486=ORIENTED_EDGE('',*,*,#3334,.F.);
#4487=ORIENTED_EDGE('',*,*,#3335,.T.);
#4488=ORIENTED_EDGE('',*,*,#3333,.T.);
#4489=ORIENTED_EDGE('',*,*,#3335,.F.);
#4490=ORIENTED_EDGE('',*,*,#3336,.F.);
#4491=ORIENTED_EDGE('',*,*,#3337,.T.);
#4492=ORIENTED_EDGE('',*,*,#3334,.T.);
#4493=ORIENTED_EDGE('',*,*,#3337,.F.);
#4494=ORIENTED_EDGE('',*,*,#3338,.F.);
#4495=ORIENTED_EDGE('',*,*,#3339,.T.);
#4496=ORIENTED_EDGE('',*,*,#3336,.T.);
#4497=ORIENTED_EDGE('',*,*,#3339,.F.);
#4498=ORIENTED_EDGE('',*,*,#3338,.T.);
#4499=ORIENTED_EDGE('',*,*,#3340,.F.);
#4500=ORIENTED_EDGE('',*,*,#3341,.F.);
#4501=ORIENTED_EDGE('',*,*,#3342,.T.);
#4502=ORIENTED_EDGE('',*,*,#3340,.T.);
#4503=ORIENTED_EDGE('',*,*,#3342,.F.);
#4504=ORIENTED_EDGE('',*,*,#3343,.F.);
#4505=ORIENTED_EDGE('',*,*,#3344,.T.);
#4506=ORIENTED_EDGE('',*,*,#3341,.T.);
#4507=ORIENTED_EDGE('',*,*,#3344,.F.);
#4508=ORIENTED_EDGE('',*,*,#3345,.F.);
#4509=ORIENTED_EDGE('',*,*,#3346,.T.);
#4510=ORIENTED_EDGE('',*,*,#3343,.T.);
#4511=ORIENTED_EDGE('',*,*,#3346,.F.);
#4512=ORIENTED_EDGE('',*,*,#3345,.T.);
#4513=ORIENTED_EDGE('',*,*,#3347,.T.);
#4514=ORIENTED_EDGE('',*,*,#3348,.T.);
#4515=ORIENTED_EDGE('',*,*,#3349,.T.);
#4516=ORIENTED_EDGE('',*,*,#3350,.F.);
#4517=ORIENTED_EDGE('',*,*,#3351,.T.);
#4518=ORIENTED_EDGE('',*,*,#3352,.T.);
#4519=ORIENTED_EDGE('',*,*,#3353,.T.);
#4520=ORIENTED_EDGE('',*,*,#3348,.F.);
#4521=ORIENTED_EDGE('',*,*,#3354,.T.);
#4522=ORIENTED_EDGE('',*,*,#3355,.T.);
#4523=ORIENTED_EDGE('',*,*,#3356,.T.);
#4524=ORIENTED_EDGE('',*,*,#3352,.F.);
#4525=ORIENTED_EDGE('',*,*,#3357,.T.);
#4526=ORIENTED_EDGE('',*,*,#3358,.T.);
#4527=ORIENTED_EDGE('',*,*,#3359,.T.);
#4528=ORIENTED_EDGE('',*,*,#3355,.F.);
#4529=ORIENTED_EDGE('',*,*,#3360,.T.);
#4530=ORIENTED_EDGE('',*,*,#3361,.T.);
#4531=ORIENTED_EDGE('',*,*,#3362,.T.);
#4532=ORIENTED_EDGE('',*,*,#3358,.F.);
#4533=ORIENTED_EDGE('',*,*,#3363,.T.);
#4534=ORIENTED_EDGE('',*,*,#3350,.T.);
#4535=ORIENTED_EDGE('',*,*,#3364,.T.);
#4536=ORIENTED_EDGE('',*,*,#3361,.F.);
#4537=ORIENTED_EDGE('',*,*,#3363,.F.);
#4538=ORIENTED_EDGE('',*,*,#3360,.F.);
#4539=ORIENTED_EDGE('',*,*,#3357,.F.);
#4540=ORIENTED_EDGE('',*,*,#3354,.F.);
#4541=ORIENTED_EDGE('',*,*,#3351,.F.);
#4542=ORIENTED_EDGE('',*,*,#3347,.F.);
#4543=ORIENTED_EDGE('',*,*,#3364,.F.);
#4544=ORIENTED_EDGE('',*,*,#3349,.F.);
#4545=ORIENTED_EDGE('',*,*,#3353,.F.);
#4546=ORIENTED_EDGE('',*,*,#3356,.F.);
#4547=ORIENTED_EDGE('',*,*,#3359,.F.);
#4548=ORIENTED_EDGE('',*,*,#3362,.F.);
#4711=CYLINDRICAL_SURFACE('',#5739,0.425);
#4712=CYLINDRICAL_SURFACE('',#5747,0.24505);
#4965=ADVANCED_FACE('',(#956),#684,.T.);
#4966=ADVANCED_FACE('',(#957),#311,.T.);
#4967=ADVANCED_FACE('',(#958),#4711,.T.);
#4968=ADVANCED_FACE('',(#959),#312,.T.);
#4969=ADVANCED_FACE('',(#960,#525),#685,.T.);
#4970=ADVANCED_FACE('',(#961),#313,.T.);
#4971=ADVANCED_FACE('',(#962),#4712,.T.);
#4972=ADVANCED_FACE('',(#963),#314,.T.);
#4973=ADVANCED_FACE('',(#964),#686,.T.);
#4974=ADVANCED_FACE('',(#965),#687,.F.);
#4975=ADVANCED_FACE('',(#966),#688,.F.);
#4976=ADVANCED_FACE('',(#967),#689,.F.);
#4977=ADVANCED_FACE('',(#968),#690,.F.);
#4978=ADVANCED_FACE('',(#969),#691,.F.);
#4979=ADVANCED_FACE('',(#970),#692,.F.);
#4980=ADVANCED_FACE('',(#971),#693,.F.);
#4981=ADVANCED_FACE('',(#972),#694,.F.);
#5029=CLOSED_SHELL('',(#4965,#4966,#4967,#4968,#4969,#4970,#4971,#4972,
#4973));
#5030=CLOSED_SHELL('',(#4974,#4975,#4976,#4977,#4978,#4979,#4980,#4981));
#5734=AXIS2_PLACEMENT_3D('',#10007,#7094,#7095);
#5735=AXIS2_PLACEMENT_3D('',#10008,#7096,#7097);
#5736=AXIS2_PLACEMENT_3D('',#10010,#7098,#7099);
#5737=AXIS2_PLACEMENT_3D('',#10011,#7100,#7101);
#5738=AXIS2_PLACEMENT_3D('',#10013,#7102,#7103);
#5739=AXIS2_PLACEMENT_3D('',#10015,#7105,#7106);
#5740=AXIS2_PLACEMENT_3D('',#10017,#7107,#7108);
#5741=AXIS2_PLACEMENT_3D('',#10019,#7110,#7111);
#5742=AXIS2_PLACEMENT_3D('',#10021,#7112,#7113);
#5743=AXIS2_PLACEMENT_3D('',#10023,#7115,#7116);
#5744=AXIS2_PLACEMENT_3D('',#10025,#7117,#7118);
#5745=AXIS2_PLACEMENT_3D('',#10026,#7119,#7120);
#5746=AXIS2_PLACEMENT_3D('',#10028,#7121,#7122);
#5747=AXIS2_PLACEMENT_3D('',#10030,#7124,#7125);
#5748=AXIS2_PLACEMENT_3D('',#10032,#7126,#7127);
#5749=AXIS2_PLACEMENT_3D('',#10034,#7129,#7130);
#5750=AXIS2_PLACEMENT_3D('',#10036,#7131,#7132);
#5751=AXIS2_PLACEMENT_3D('',#10038,#7134,#7135);
#5752=AXIS2_PLACEMENT_3D('',#10039,#7136,#7137);
#5753=AXIS2_PLACEMENT_3D('',#10048,#7142,#7143);
#5754=AXIS2_PLACEMENT_3D('',#10054,#7147,#7148);
#5755=AXIS2_PLACEMENT_3D('',#10060,#7152,#7153);
#5756=AXIS2_PLACEMENT_3D('',#10066,#7157,#7158);
#5757=AXIS2_PLACEMENT_3D('',#10072,#7162,#7163);
#5758=AXIS2_PLACEMENT_3D('',#10075,#7166,#7167);
#5759=AXIS2_PLACEMENT_3D('',#10076,#7168,#7169);
#7094=DIRECTION('axis',(0.,0.,1.));
#7095=DIRECTION('refdir',(1.,0.,0.));
#7096=DIRECTION('center_axis',(0.,1.,0.));
#7097=DIRECTION('ref_axis',(0.,0.,1.));
#7098=DIRECTION('center_axis',(0.,-1.,0.));
#7099=DIRECTION('ref_axis',(1.,0.,0.));
#7100=DIRECTION('center_axis',(0.,-1.,0.));
#7101=DIRECTION('ref_axis',(1.,0.,0.));
#7102=DIRECTION('center_axis',(0.,-1.,0.));
#7103=DIRECTION('ref_axis',(1.,0.,0.));
#7104=DIRECTION('',(0.707106781186548,0.707106781186547,8.65956056235493E-17));
#7105=DIRECTION('center_axis',(0.,-1.,0.));
#7106=DIRECTION('ref_axis',(1.,0.,0.));
#7107=DIRECTION('center_axis',(0.,-1.,0.));
#7108=DIRECTION('ref_axis',(1.,0.,0.));
#7109=DIRECTION('',(0.,1.,0.));
#7110=DIRECTION('center_axis',(0.,1.,0.));
#7111=DIRECTION('ref_axis',(1.,0.,0.));
#7112=DIRECTION('center_axis',(0.,-1.,0.));
#7113=DIRECTION('ref_axis',(1.,0.,0.));
#7114=DIRECTION('',(-0.707106781186547,0.707106781186548,-8.65956056235493E-17));
#7115=DIRECTION('center_axis',(0.,-1.,0.));
#7116=DIRECTION('ref_axis',(0.,0.,-1.));
#7117=DIRECTION('center_axis',(0.,-1.,0.));
#7118=DIRECTION('ref_axis',(1.,0.,0.));
#7119=DIRECTION('center_axis',(0.,1.,0.));
#7120=DIRECTION('ref_axis',(1.,0.,0.));
#7121=DIRECTION('center_axis',(0.,1.,0.));
#7122=DIRECTION('ref_axis',(1.,0.,0.));
#7123=DIRECTION('',(-0.447213595499958,0.894427190999916,-5.47678698264203E-17));
#7124=DIRECTION('center_axis',(0.,-1.,0.));
#7125=DIRECTION('ref_axis',(1.,0.,0.));
#7126=DIRECTION('center_axis',(0.,1.,0.));
#7127=DIRECTION('ref_axis',(1.,0.,0.));
#7128=DIRECTION('',(0.,1.,0.));
#7129=DIRECTION('center_axis',(0.,1.,0.));
#7130=DIRECTION('ref_axis',(1.,0.,0.));
#7131=DIRECTION('center_axis',(0.,-1.,0.));
#7132=DIRECTION('ref_axis',(1.,0.,0.));
#7133=DIRECTION('',(-0.707106781186547,0.707106781186548,-8.65956056235493E-17));
#7134=DIRECTION('center_axis',(0.,-1.,0.));
#7135=DIRECTION('ref_axis',(0.,0.,-1.));
#7136=DIRECTION('center_axis',(0.866025403784439,0.,-0.5));
#7137=DIRECTION('ref_axis',(0.5,0.,0.866025403784439));
#7138=DIRECTION('',(-0.5,0.,-0.866025403784439));
#7139=DIRECTION('',(0.,-1.,0.));
#7140=DIRECTION('',(0.5,0.,0.866025403784439));
#7141=DIRECTION('',(0.,-1.,0.));
#7142=DIRECTION('center_axis',(1.20185167898973E-16,0.,-1.));
#7143=DIRECTION('ref_axis',(1.,0.,1.20185167898973E-16));
#7144=DIRECTION('',(-1.,0.,-1.20185167898973E-16));
#7145=DIRECTION('',(0.,-1.,0.));
#7146=DIRECTION('',(1.,0.,1.20185167898973E-16));
#7147=DIRECTION('center_axis',(-0.866025403784439,0.,-0.5));
#7148=DIRECTION('ref_axis',(0.5,0.,-0.866025403784439));
#7149=DIRECTION('',(-0.5,0.,0.866025403784439));
#7150=DIRECTION('',(0.,-1.,0.));
#7151=DIRECTION('',(0.5,0.,-0.866025403784439));
#7152=DIRECTION('center_axis',(-0.866025403784439,0.,0.5));
#7153=DIRECTION('ref_axis',(-0.5,0.,-0.866025403784439));
#7154=DIRECTION('',(0.5,0.,0.866025403784439));
#7155=DIRECTION('',(0.,-1.,0.));
#7156=DIRECTION('',(-0.5,0.,-0.866025403784439));
#7157=DIRECTION('center_axis',(-2.40370335797945E-16,0.,1.));
#7158=DIRECTION('ref_axis',(-1.,0.,-2.40370335797945E-16));
#7159=DIRECTION('',(1.,0.,2.40370335797945E-16));
#7160=DIRECTION('',(0.,-1.,0.));
#7161=DIRECTION('',(-1.,0.,-2.40370335797945E-16));
#7162=DIRECTION('center_axis',(0.866025403784439,0.,0.5));
#7163=DIRECTION('ref_axis',(-0.5,0.,0.866025403784439));
#7164=DIRECTION('',(0.5,0.,-0.866025403784439));
#7165=DIRECTION('',(-0.5,0.,0.866025403784439));
#7166=DIRECTION('center_axis',(0.,1.,0.));
#7167=DIRECTION('ref_axis',(1.,0.,0.));
#7168=DIRECTION('center_axis',(0.,-1.,0.));
#7169=DIRECTION('ref_axis',(0.,0.,-1.));
#10007=CARTESIAN_POINT('',(0.,0.,0.));
#10008=CARTESIAN_POINT('Origin',(0.375,0.5,0.));
#10009=CARTESIAN_POINT('',(-0.375,0.5,-4.59242549680257E-17));
#10010=CARTESIAN_POINT('Origin',(0.,0.5,0.));
#10011=CARTESIAN_POINT('Origin',(0.,0.475,0.));
#10012=CARTESIAN_POINT('',(-0.425,0.45,-5.20474889637625E-17));
#10013=CARTESIAN_POINT('Origin',(0.,0.45,0.));
#10014=CARTESIAN_POINT('',(-0.4,0.475,-4.89858719658941E-17));
#10015=CARTESIAN_POINT('Origin',(0.,0.24,0.));
#10016=CARTESIAN_POINT('',(-0.425,0.0299999999999998,-5.20474889637625E-17));
#10017=CARTESIAN_POINT('Origin',(0.,0.0299999999999998,0.));
#10018=CARTESIAN_POINT('',(-0.425,0.24,-5.20474889637625E-17));
#10019=CARTESIAN_POINT('Origin',(0.,0.0150000000000001,0.));
#10020=CARTESIAN_POINT('',(-0.395,4.85722573273506E-17,-4.83735485663204E-17));
#10021=CARTESIAN_POINT('Origin',(0.,0.,0.));
#10022=CARTESIAN_POINT('',(-0.41,0.0150000000000001,-5.02105187650415E-17));
#10023=CARTESIAN_POINT('Origin',(0.27,0.,0.));
#10024=CARTESIAN_POINT('',(-0.27,0.,-3.30654635769785E-17));
#10025=CARTESIAN_POINT('Origin',(0.,0.,0.));
#10026=CARTESIAN_POINT('Origin',(0.,-0.02,0.));
#10027=CARTESIAN_POINT('',(-0.24505,-0.0498999999999999,3.00099698131059E-17));
#10028=CARTESIAN_POINT('Origin',(0.,-0.0498999999999999,0.));
#10029=CARTESIAN_POINT('',(-0.26,-0.02,-3.18408167778312E-17));
#10030=CARTESIAN_POINT('Origin',(0.,-0.995,0.));
#10031=CARTESIAN_POINT('',(-0.24505,-1.95495,3.00099698131059E-17));
#10032=CARTESIAN_POINT('Origin',(0.,-1.95495,0.));
#10033=CARTESIAN_POINT('',(-0.24505,-0.995,-3.00099698131059E-17));
#10034=CARTESIAN_POINT('Origin',(0.,-1.975,0.));
#10035=CARTESIAN_POINT('',(-0.2,-2.,-2.44929359829471E-17));
#10036=CARTESIAN_POINT('Origin',(0.,-2.,0.));
#10037=CARTESIAN_POINT('',(-0.225,-1.975,-2.75545529808154E-17));
#10038=CARTESIAN_POINT('Origin',(0.,-2.,0.));
#10039=CARTESIAN_POINT('Origin',(0.115470053837925,-0.5,-0.2));
#10040=CARTESIAN_POINT('',(0.23094010767585,-0.5,0.));
#10041=CARTESIAN_POINT('',(0.115470053837925,-0.5,-0.2));
#10042=CARTESIAN_POINT('',(0.23094010767585,-0.5,0.));
#10043=CARTESIAN_POINT('',(0.115470053837925,-0.8,-0.2));
#10044=CARTESIAN_POINT('',(0.115470053837925,-0.5,-0.2));
#10045=CARTESIAN_POINT('',(0.23094010767585,-0.8,0.));
#10046=CARTESIAN_POINT('',(0.23094010767585,-0.8,0.));
#10047=CARTESIAN_POINT('',(0.23094010767585,-0.5,0.));
#10048=CARTESIAN_POINT('Origin',(-0.115470053837925,-0.5,-0.2));
#10049=CARTESIAN_POINT('',(-0.115470053837925,-0.5,-0.2));
#10050=CARTESIAN_POINT('',(0.115470053837925,-0.5,-0.2));
#10051=CARTESIAN_POINT('',(-0.115470053837925,-0.8,-0.2));
#10052=CARTESIAN_POINT('',(-0.115470053837925,-0.5,-0.2));
#10053=CARTESIAN_POINT('',(0.115470053837925,-0.8,-0.2));
#10054=CARTESIAN_POINT('Origin',(-0.23094010767585,-0.5,-2.77555756156289E-17));
#10055=CARTESIAN_POINT('',(-0.23094010767585,-0.5,-2.82820063659975E-17));
#10056=CARTESIAN_POINT('',(-0.115470053837925,-0.5,-0.2));
#10057=CARTESIAN_POINT('',(-0.23094010767585,-0.8,-2.77555756156289E-17));
#10058=CARTESIAN_POINT('',(-0.23094010767585,-0.5,-2.82820063659975E-17));
#10059=CARTESIAN_POINT('',(-0.115470053837925,-0.8,-0.2));
#10060=CARTESIAN_POINT('Origin',(-0.115470053837925,-0.5,0.2));
#10061=CARTESIAN_POINT('',(-0.115470053837925,-0.5,0.2));
#10062=CARTESIAN_POINT('',(-0.23094010767585,-0.5,-2.82820063659975E-17));
#10063=CARTESIAN_POINT('',(-0.115470053837925,-0.8,0.2));
#10064=CARTESIAN_POINT('',(-0.115470053837925,-0.5,0.2));
#10065=CARTESIAN_POINT('',(-0.23094010767585,-0.8,-2.82820063659975E-17));
#10066=CARTESIAN_POINT('Origin',(0.115470053837925,-0.5,0.2));
#10067=CARTESIAN_POINT('',(0.115470053837925,-0.5,0.2));
#10068=CARTESIAN_POINT('',(-0.115470053837925,-0.5,0.2));
#10069=CARTESIAN_POINT('',(0.115470053837925,-0.8,0.2));
#10070=CARTESIAN_POINT('',(0.115470053837925,-0.5,0.2));
#10071=CARTESIAN_POINT('',(-0.115470053837925,-0.8,0.2));
#10072=CARTESIAN_POINT('Origin',(0.23094010767585,-0.5,0.));
#10073=CARTESIAN_POINT('',(0.115470053837925,-0.5,0.2));
#10074=CARTESIAN_POINT('',(0.115470053837925,-0.8,0.2));
#10075=CARTESIAN_POINT('Origin',(0.,-0.5,0.));
#10076=CARTESIAN_POINT('Origin',(0.,-0.8,0.));
#10260=UNCERTAINTY_MEASURE_WITH_UNIT(LENGTH_MEASURE(0.001),#10293,
'DISTANCE_ACCURACY_VALUE',
'Maximum model space distance between geometric entities at asserted c
onnectivities');
#10264=UNCERTAINTY_MEASURE_WITH_UNIT(LENGTH_MEASURE(0.001),#10293,
'DISTANCE_ACCURACY_VALUE',
'Maximum model space distance between geometric entities at asserted c
onnectivities');
#10288=(
GEOMETRIC_REPRESENTATION_CONTEXT(3)
GLOBAL_UNCERTAINTY_ASSIGNED_CONTEXT((#10260))
GLOBAL_UNIT_ASSIGNED_CONTEXT((#10293,#10295,#10296))
REPRESENTATION_CONTEXT('','3D')
);
#10292=(
GEOMETRIC_REPRESENTATION_CONTEXT(3)
GLOBAL_UNCERTAINTY_ASSIGNED_CONTEXT((#10264))
GLOBAL_UNIT_ASSIGNED_CONTEXT((#10293,#10295,#10296))
REPRESENTATION_CONTEXT('','3D')
);
#10293=(
LENGTH_UNIT()
NAMED_UNIT(*)
SI_UNIT(.CENTI.,.METRE.)
);
#10295=(
NAMED_UNIT(*)
PLANE_ANGLE_UNIT()
SI_UNIT($,.RADIAN.)
);
#10296=(
NAMED_UNIT(*)
SI_UNIT($,.STERADIAN.)
SOLID_ANGLE_UNIT()
);
#10320=SHAPE_DEFINITION_REPRESENTATION(#10349,#10436);
#10349=PRODUCT_DEFINITION_SHAPE('',$,#10464);
#10436=SHAPE_REPRESENTATION('',(#5734),#10288);
#10440=PRODUCT_DEFINITION_CONTEXT('part definition',#10523,'design');
#10464=PRODUCT_DEFINITION('Cap Screw - M5x20','Cap Screw - M5x20',
#10491,#10440);
#10491=PRODUCT_DEFINITION_FORMATION('',$,#10548);
#10523=APPLICATION_CONTEXT(
'Core Data for Automotive Mechanical Design Process');
#10524=PRODUCT_CONTEXT('part definition',#10523,'mechanical');
#10548=PRODUCT('Cap Screw - M5x20','Cap Screw - M5x20',
'Cap Screw - M5x20',(#10524));
#10629=COLOUR_RGB('Black',0.12,0.14,0.17);
#10630=FILL_AREA_STYLE_COLOUR('',#10629);
#10631=FILL_AREA_STYLE('',(#10630));
#10632=SURFACE_STYLE_FILL_AREA(#10631);
#10633=SURFACE_SIDE_STYLE('',(#10632));
#10634=SURFACE_STYLE_USAGE(.BOTH.,#10633);
#10635=PRESENTATION_STYLE_ASSIGNMENT((#10634));
ENDSEC;
END-ISO-10303-21;
